ISO-10303-21;
HEADER;
/* Generated by software containing ST-Developer
 * from STEP Tools, Inc. (www.steptools.com) 
 */

FILE_DESCRIPTION(
/* description */ ('STEP AP214'),
/* implementation_level */ '2;1');

FILE_NAME(
/* name */ 'socket head cap screw_iso_ISO 4762 M5 x 20 - 20N.step',
/* time_stamp */ '2026-11-04T19:00:26-08:00',
/* author */ (''),
/* organization */ (''),
/* preprocessor_version */ 'ST-DEVELOPER v20.2',
/* originating_system */ 'Autodesk Translation Framework v15.17.0.0',
/* authorisation */ '');

FILE_SCHEMA (('AUTOMOTIVE_DESIGN { 1 0 10303 214 3 1 1 }'));
ENDSEC;

DATA;
#10=MECHANICAL_DESIGN_GEOMETRIC_PRESENTATION_REPRESENTATION('',(#276),#5689);
#237=CONICAL_SURFACE('',#3247,2.042,1.04719755119659);
#238=CONICAL_SURFACE('',#3267,2.055,0.785398163397472);
#254=TOROIDAL_SURFACE('',#3254,4.,0.25);
#255=TOROIDAL_SURFACE('',#3258,2.7,0.2);
#262=SHAPE_REPRESENTATION_RELATIONSHIP('SRR','None',#5763,#269);
#269=ADVANCED_BREP_SHAPE_REPRESENTATION('',(#283),#5687);
#276=STYLED_ITEM('',(#5806),#283);
#283=MANIFOLD_SOLID_BREP('Body1',#2966);
#339=FACE_BOUND('',#774,.T.);
#340=FACE_BOUND('',#777,.T.);
#419=PLANE('',#3269);
#420=PLANE('',#3270);
#421=PLANE('',#3271);
#422=PLANE('',#3272);
#423=PLANE('',#3273);
#424=PLANE('',#3274);
#425=PLANE('',#3275);
#426=PLANE('',#3276);
#427=PLANE('',#3277);
#428=PLANE('',#3278);
#429=PLANE('',#3279);
#430=PLANE('',#3280);
#431=PLANE('',#3281);
#432=PLANE('',#3282);
#433=PLANE('',#3283);
#554=FACE_OUTER_BOUND('',#767,.T.);
#555=FACE_OUTER_BOUND('',#768,.T.);
#556=FACE_OUTER_BOUND('',#769,.T.);
#557=FACE_OUTER_BOUND('',#770,.T.);
#558=FACE_OUTER_BOUND('',#771,.T.);
#559=FACE_OUTER_BOUND('',#772,.T.);
#560=FACE_OUTER_BOUND('',#773,.T.);
#561=FACE_OUTER_BOUND('',#775,.T.);
#562=FACE_OUTER_BOUND('',#776,.T.);
#563=FACE_OUTER_BOUND('',#778,.T.);
#564=FACE_OUTER_BOUND('',#779,.T.);
#565=FACE_OUTER_BOUND('',#780,.T.);
#566=FACE_OUTER_BOUND('',#781,.T.);
#567=FACE_OUTER_BOUND('',#782,.T.);
#568=FACE_OUTER_BOUND('',#783,.T.);
#569=FACE_OUTER_BOUND('',#784,.T.);
#570=FACE_OUTER_BOUND('',#785,.T.);
#571=FACE_OUTER_BOUND('',#786,.T.);
#572=FACE_OUTER_BOUND('',#787,.T.);
#573=FACE_OUTER_BOUND('',#788,.T.);
#574=FACE_OUTER_BOUND('',#789,.T.);
#767=EDGE_LOOP('',(#2560,#2561,#2562,#2563,#2564,#2565,#2566,#2567));
#768=EDGE_LOOP('',(#2568,#2569,#2570,#2571));
#769=EDGE_LOOP('',(#2572,#2573,#2574,#2575,#2576));
#770=EDGE_LOOP('',(#2577,#2578,#2579,#2580));
#771=EDGE_LOOP('',(#2581,#2582,#2583,#2584,#2585));
#772=EDGE_LOOP('',(#2586,#2587,#2588,#2589));
#773=EDGE_LOOP('',(#2590));
#774=EDGE_LOOP('',(#2591,#2592,#2593,#2594,#2595,#2596));
#775=EDGE_LOOP('',(#2597));
#776=EDGE_LOOP('',(#2598));
#777=EDGE_LOOP('',(#2599));
#778=EDGE_LOOP('',(#2600,#2601,#2602,#2603,#2604));
#779=EDGE_LOOP('',(#2605,#2606,#2607,#2608,#2609));
#780=EDGE_LOOP('',(#2610,#2611,#2612,#2613,#2614));
#781=EDGE_LOOP('',(#2615,#2616,#2617,#2618,#2619));
#782=EDGE_LOOP('',(#2620,#2621,#2622,#2623,#2624));
#783=EDGE_LOOP('',(#2625,#2626,#2627,#2628,#2629));
#784=EDGE_LOOP('',(#2630,#2631,#2632));
#785=EDGE_LOOP('',(#2633,#2634,#2635));
#786=EDGE_LOOP('',(#2636,#2637,#2638));
#787=EDGE_LOOP('',(#2639,#2640,#2641));
#788=EDGE_LOOP('',(#2642,#2643,#2644));
#789=EDGE_LOOP('',(#2645,#2646,#2647));
#1010=LINE('',#4818,#1241);
#1011=LINE('',#4846,#1242);
#1012=LINE('',#4850,#1243);
#1013=LINE('',#4854,#1244);
#1014=LINE('',#4859,#1245);
#1015=LINE('',#4861,#1246);
#1016=LINE('',#4863,#1247);
#1017=LINE('',#4865,#1248);
#1018=LINE('',#4867,#1249);
#1019=LINE('',#4868,#1250);
#1020=LINE('',#4873,#1251);
#1021=LINE('',#4874,#1252);
#1022=LINE('',#4876,#1253);
#1023=LINE('',#4877,#1254);
#1024=LINE('',#4879,#1255);
#1025=LINE('',#4881,#1256);
#1026=LINE('',#4882,#1257);
#1027=LINE('',#4884,#1258);
#1028=LINE('',#4886,#1259);
#1029=LINE('',#4887,#1260);
#1030=LINE('',#4889,#1261);
#1031=LINE('',#4891,#1262);
#1032=LINE('',#4892,#1263);
#1033=LINE('',#4894,#1264);
#1034=LINE('',#4896,#1265);
#1035=LINE('',#4897,#1266);
#1036=LINE('',#4899,#1267);
#1037=LINE('',#4900,#1268);
#1241=VECTOR('',#3965,2.042);
#1242=VECTOR('',#3998,4.25);
#1243=VECTOR('',#4003,2.5);
#1244=VECTOR('',#4008,2.055);
#1245=VECTOR('',#4013,1000.);
#1246=VECTOR('',#4014,1000.);
#1247=VECTOR('',#4015,1000.);
#1248=VECTOR('',#4016,1000.);
#1249=VECTOR('',#4017,1000.);
#1250=VECTOR('',#4018,1000.);
#1251=VECTOR('',#4025,1000.);
#1252=VECTOR('',#4026,1000.);
#1253=VECTOR('',#4027,1000.);
#1254=VECTOR('',#4028,1000.);
#1255=VECTOR('',#4031,1000.);
#1256=VECTOR('',#4032,1000.);
#1257=VECTOR('',#4033,1000.);
#1258=VECTOR('',#4036,1000.);
#1259=VECTOR('',#4037,1000.);
#1260=VECTOR('',#4038,1000.);
#1261=VECTOR('',#4041,1000.);
#1262=VECTOR('',#4042,1000.);
#1263=VECTOR('',#4043,1000.);
#1264=VECTOR('',#4046,1000.);
#1265=VECTOR('',#4047,1000.);
#1266=VECTOR('',#4048,1000.);
#1267=VECTOR('',#4051,1000.);
#1268=VECTOR('',#4052,1000.);
#1362=CIRCLE('',#3248,2.042);
#1363=CIRCLE('',#3249,2.042);
#1364=CIRCLE('',#3250,2.042);
#1365=CIRCLE('',#3251,2.042);
#1366=CIRCLE('',#3252,2.042);
#1367=CIRCLE('',#3253,2.042);
#1368=CIRCLE('',#3255,4.);
#1369=CIRCLE('',#3256,0.25);
#1370=CIRCLE('',#3257,4.25);
#1371=CIRCLE('',#3259,2.5);
#1372=CIRCLE('',#3260,2.5);
#1373=CIRCLE('',#3261,0.2);
#1374=CIRCLE('',#3262,2.7);
#1375=CIRCLE('',#3264,4.25);
#1376=CIRCLE('',#3266,2.5);
#1377=CIRCLE('',#3268,2.055);
#1571=VERTEX_POINT('',#4816);
#1572=VERTEX_POINT('',#4817);
#1573=VERTEX_POINT('',#4819);
#1574=VERTEX_POINT('',#4821);
#1575=VERTEX_POINT('',#4823);
#1576=VERTEX_POINT('',#4825);
#1577=VERTEX_POINT('',#4827);
#1578=VERTEX_POINT('',#4831);
#1579=VERTEX_POINT('',#4833);
#1580=VERTEX_POINT('',#4837);
#1581=VERTEX_POINT('',#4838);
#1582=VERTEX_POINT('',#4841);
#1583=VERTEX_POINT('',#4845);
#1584=VERTEX_POINT('',#4849);
#1585=VERTEX_POINT('',#4853);
#1586=VERTEX_POINT('',#4857);
#1587=VERTEX_POINT('',#4858);
#1588=VERTEX_POINT('',#4860);
#1589=VERTEX_POINT('',#4862);
#1590=VERTEX_POINT('',#4864);
#1591=VERTEX_POINT('',#4866);
#1592=VERTEX_POINT('',#4872);
#1593=VERTEX_POINT('',#4875);
#1594=VERTEX_POINT('',#4880);
#1595=VERTEX_POINT('',#4885);
#1596=VERTEX_POINT('',#4890);
#1597=VERTEX_POINT('',#4895);
#1908=EDGE_CURVE('',#1571,#1572,#1010,.T.);
#1909=EDGE_CURVE('',#1572,#1573,#1362,.T.);
#1910=EDGE_CURVE('',#1573,#1574,#1363,.T.);
#1911=EDGE_CURVE('',#1574,#1575,#1364,.T.);
#1912=EDGE_CURVE('',#1575,#1576,#1365,.T.);
#1913=EDGE_CURVE('',#1576,#1577,#1366,.T.);
#1914=EDGE_CURVE('',#1577,#1572,#1367,.T.);
#1915=EDGE_CURVE('',#1578,#1578,#1368,.T.);
#1916=EDGE_CURVE('',#1578,#1579,#1369,.T.);
#1917=EDGE_CURVE('',#1579,#1579,#1370,.T.);
#1918=EDGE_CURVE('',#1580,#1581,#1371,.T.);
#1919=EDGE_CURVE('',#1581,#1580,#1372,.T.);
#1920=EDGE_CURVE('',#1581,#1582,#1373,.T.);
#1921=EDGE_CURVE('',#1582,#1582,#1374,.T.);
#1922=EDGE_CURVE('',#1579,#1583,#1011,.T.);
#1923=EDGE_CURVE('',#1583,#1583,#1375,.T.);
#1924=EDGE_CURVE('',#1580,#1584,#1012,.T.);
#1925=EDGE_CURVE('',#1584,#1584,#1376,.T.);
#1926=EDGE_CURVE('',#1584,#1585,#1013,.T.);
#1927=EDGE_CURVE('',#1585,#1585,#1377,.T.);
#1928=EDGE_CURVE('',#1586,#1587,#1014,.T.);
#1929=EDGE_CURVE('',#1588,#1587,#1015,.T.);
#1930=EDGE_CURVE('',#1588,#1589,#1016,.T.);
#1931=EDGE_CURVE('',#1589,#1590,#1017,.T.);
#1932=EDGE_CURVE('',#1591,#1590,#1018,.T.);
#1933=EDGE_CURVE('',#1586,#1591,#1019,.T.);
#1934=EDGE_CURVE('',#1592,#1586,#1020,.T.);
#1935=EDGE_CURVE('',#1592,#1576,#1021,.T.);
#1936=EDGE_CURVE('',#1576,#1593,#1022,.T.);
#1937=EDGE_CURVE('',#1593,#1587,#1023,.T.);
#1938=EDGE_CURVE('',#1575,#1593,#1024,.T.);
#1939=EDGE_CURVE('',#1594,#1575,#1025,.T.);
#1940=EDGE_CURVE('',#1594,#1588,#1026,.T.);
#1941=EDGE_CURVE('',#1594,#1574,#1027,.T.);
#1942=EDGE_CURVE('',#1574,#1595,#1028,.T.);
#1943=EDGE_CURVE('',#1595,#1589,#1029,.T.);
#1944=EDGE_CURVE('',#1595,#1573,#1030,.T.);
#1945=EDGE_CURVE('',#1573,#1596,#1031,.T.);
#1946=EDGE_CURVE('',#1596,#1590,#1032,.T.);
#1947=EDGE_CURVE('',#1572,#1596,#1033,.T.);
#1948=EDGE_CURVE('',#1597,#1572,#1034,.T.);
#1949=EDGE_CURVE('',#1597,#1591,#1035,.T.);
#1950=EDGE_CURVE('',#1577,#1597,#1036,.T.);
#1951=EDGE_CURVE('',#1592,#1577,#1037,.T.);
#2560=ORIENTED_EDGE('',*,*,#1908,.T.);
#2561=ORIENTED_EDGE('',*,*,#1909,.T.);
#2562=ORIENTED_EDGE('',*,*,#1910,.T.);
#2563=ORIENTED_EDGE('',*,*,#1911,.T.);
#2564=ORIENTED_EDGE('',*,*,#1912,.T.);
#2565=ORIENTED_EDGE('',*,*,#1913,.T.);
#2566=ORIENTED_EDGE('',*,*,#1914,.T.);
#2567=ORIENTED_EDGE('',*,*,#1908,.F.);
#2568=ORIENTED_EDGE('',*,*,#1915,.F.);
#2569=ORIENTED_EDGE('',*,*,#1916,.T.);
#2570=ORIENTED_EDGE('',*,*,#1917,.F.);
#2571=ORIENTED_EDGE('',*,*,#1916,.F.);
#2572=ORIENTED_EDGE('',*,*,#1918,.F.);
#2573=ORIENTED_EDGE('',*,*,#1919,.F.);
#2574=ORIENTED_EDGE('',*,*,#1920,.T.);
#2575=ORIENTED_EDGE('',*,*,#1921,.F.);
#2576=ORIENTED_EDGE('',*,*,#1920,.F.);
#2577=ORIENTED_EDGE('',*,*,#1917,.T.);
#2578=ORIENTED_EDGE('',*,*,#1922,.T.);
#2579=ORIENTED_EDGE('',*,*,#1923,.T.);
#2580=ORIENTED_EDGE('',*,*,#1922,.F.);
#2581=ORIENTED_EDGE('',*,*,#1918,.T.);
#2582=ORIENTED_EDGE('',*,*,#1919,.T.);
#2583=ORIENTED_EDGE('',*,*,#1924,.T.);
#2584=ORIENTED_EDGE('',*,*,#1925,.T.);
#2585=ORIENTED_EDGE('',*,*,#1924,.F.);
#2586=ORIENTED_EDGE('',*,*,#1925,.F.);
#2587=ORIENTED_EDGE('',*,*,#1926,.T.);
#2588=ORIENTED_EDGE('',*,*,#1927,.T.);
#2589=ORIENTED_EDGE('',*,*,#1926,.F.);
#2590=ORIENTED_EDGE('',*,*,#1915,.T.);
#2591=ORIENTED_EDGE('',*,*,#1928,.T.);
#2592=ORIENTED_EDGE('',*,*,#1929,.F.);
#2593=ORIENTED_EDGE('',*,*,#1930,.T.);
#2594=ORIENTED_EDGE('',*,*,#1931,.T.);
#2595=ORIENTED_EDGE('',*,*,#1932,.F.);
#2596=ORIENTED_EDGE('',*,*,#1933,.F.);
#2597=ORIENTED_EDGE('',*,*,#1927,.F.);
#2598=ORIENTED_EDGE('',*,*,#1923,.F.);
#2599=ORIENTED_EDGE('',*,*,#1921,.T.);
#2600=ORIENTED_EDGE('',*,*,#1928,.F.);
#2601=ORIENTED_EDGE('',*,*,#1934,.F.);
#2602=ORIENTED_EDGE('',*,*,#1935,.T.);
#2603=ORIENTED_EDGE('',*,*,#1936,.T.);
#2604=ORIENTED_EDGE('',*,*,#1937,.T.);
#2605=ORIENTED_EDGE('',*,*,#1929,.T.);
#2606=ORIENTED_EDGE('',*,*,#1937,.F.);
#2607=ORIENTED_EDGE('',*,*,#1938,.F.);
#2608=ORIENTED_EDGE('',*,*,#1939,.F.);
#2609=ORIENTED_EDGE('',*,*,#1940,.T.);
#2610=ORIENTED_EDGE('',*,*,#1930,.F.);
#2611=ORIENTED_EDGE('',*,*,#1940,.F.);
#2612=ORIENTED_EDGE('',*,*,#1941,.T.);
#2613=ORIENTED_EDGE('',*,*,#1942,.T.);
#2614=ORIENTED_EDGE('',*,*,#1943,.T.);
#2615=ORIENTED_EDGE('',*,*,#1931,.F.);
#2616=ORIENTED_EDGE('',*,*,#1943,.F.);
#2617=ORIENTED_EDGE('',*,*,#1944,.T.);
#2618=ORIENTED_EDGE('',*,*,#1945,.T.);
#2619=ORIENTED_EDGE('',*,*,#1946,.T.);
#2620=ORIENTED_EDGE('',*,*,#1932,.T.);
#2621=ORIENTED_EDGE('',*,*,#1946,.F.);
#2622=ORIENTED_EDGE('',*,*,#1947,.F.);
#2623=ORIENTED_EDGE('',*,*,#1948,.F.);
#2624=ORIENTED_EDGE('',*,*,#1949,.T.);
#2625=ORIENTED_EDGE('',*,*,#1933,.T.);
#2626=ORIENTED_EDGE('',*,*,#1949,.F.);
#2627=ORIENTED_EDGE('',*,*,#1950,.F.);
#2628=ORIENTED_EDGE('',*,*,#1951,.F.);
#2629=ORIENTED_EDGE('',*,*,#1934,.T.);
#2630=ORIENTED_EDGE('',*,*,#1947,.T.);
#2631=ORIENTED_EDGE('',*,*,#1945,.F.);
#2632=ORIENTED_EDGE('',*,*,#1909,.F.);
#2633=ORIENTED_EDGE('',*,*,#1944,.F.);
#2634=ORIENTED_EDGE('',*,*,#1942,.F.);
#2635=ORIENTED_EDGE('',*,*,#1910,.F.);
#2636=ORIENTED_EDGE('',*,*,#1941,.F.);
#2637=ORIENTED_EDGE('',*,*,#1939,.T.);
#2638=ORIENTED_EDGE('',*,*,#1911,.F.);
#2639=ORIENTED_EDGE('',*,*,#1938,.T.);
#2640=ORIENTED_EDGE('',*,*,#1936,.F.);
#2641=ORIENTED_EDGE('',*,*,#1912,.F.);
#2642=ORIENTED_EDGE('',*,*,#1935,.F.);
#2643=ORIENTED_EDGE('',*,*,#1951,.T.);
#2644=ORIENTED_EDGE('',*,*,#1913,.F.);
#2645=ORIENTED_EDGE('',*,*,#1950,.T.);
#2646=ORIENTED_EDGE('',*,*,#1948,.T.);
#2647=ORIENTED_EDGE('',*,*,#1914,.F.);
#2798=CYLINDRICAL_SURFACE('',#3263,4.25);
#2799=CYLINDRICAL_SURFACE('',#3265,2.5);
#2914=ADVANCED_FACE('',(#554),#237,.F.);
#2915=ADVANCED_FACE('',(#555),#254,.T.);
#2916=ADVANCED_FACE('',(#556),#255,.F.);
#2917=ADVANCED_FACE('',(#557),#2798,.T.);
#2918=ADVANCED_FACE('',(#558),#2799,.T.);
#2919=ADVANCED_FACE('',(#559),#238,.T.);
#2920=ADVANCED_FACE('',(#560,#339),#419,.T.);
#2921=ADVANCED_FACE('',(#561),#420,.T.);
#2922=ADVANCED_FACE('',(#562,#340),#421,.T.);
#2923=ADVANCED_FACE('',(#563),#422,.T.);
#2924=ADVANCED_FACE('',(#564),#423,.F.);
#2925=ADVANCED_FACE('',(#565),#424,.T.);
#2926=ADVANCED_FACE('',(#566),#425,.T.);
#2927=ADVANCED_FACE('',(#567),#426,.F.);
#2928=ADVANCED_FACE('',(#568),#427,.F.);
#2929=ADVANCED_FACE('',(#569),#428,.F.);
#2930=ADVANCED_FACE('',(#570),#429,.F.);
#2931=ADVANCED_FACE('',(#571),#430,.F.);
#2932=ADVANCED_FACE('',(#572),#431,.F.);
#2933=ADVANCED_FACE('',(#573),#432,.F.);
#2934=ADVANCED_FACE('',(#574),#433,.F.);
#2966=CLOSED_SHELL('',(#2914,#2915,#2916,#2917,#2918,#2919,#2920,#2921,
#2922,#2923,#2924,#2925,#2926,#2927,#2928,#2929,#2930,#2931,#2932,#2933,
#2934));
#3246=AXIS2_PLACEMENT_3D('',#4814,#3961,#3962);
#3247=AXIS2_PLACEMENT_3D('',#4815,#3963,#3964);
#3248=AXIS2_PLACEMENT_3D('',#4820,#3966,#3967);
#3249=AXIS2_PLACEMENT_3D('',#4822,#3968,#3969);
#3250=AXIS2_PLACEMENT_3D('',#4824,#3970,#3971);
#3251=AXIS2_PLACEMENT_3D('',#4826,#3972,#3973);
#3252=AXIS2_PLACEMENT_3D('',#4828,#3974,#3975);
#3253=AXIS2_PLACEMENT_3D('',#4829,#3976,#3977);
#3254=AXIS2_PLACEMENT_3D('',#4830,#3978,#3979);
#3255=AXIS2_PLACEMENT_3D('',#4832,#3980,#3981);
#3256=AXIS2_PLACEMENT_3D('',#4834,#3982,#3983);
#3257=AXIS2_PLACEMENT_3D('',#4835,#3984,#3985);
#3258=AXIS2_PLACEMENT_3D('',#4836,#3986,#3987);
#3259=AXIS2_PLACEMENT_3D('',#4839,#3988,#3989);
#3260=AXIS2_PLACEMENT_3D('',#4840,#3990,#3991);
#3261=AXIS2_PLACEMENT_3D('',#4842,#3992,#3993);
#3262=AXIS2_PLACEMENT_3D('',#4843,#3994,#3995);
#3263=AXIS2_PLACEMENT_3D('',#4844,#3996,#3997);
#3264=AXIS2_PLACEMENT_3D('',#4847,#3999,#4000);
#3265=AXIS2_PLACEMENT_3D('',#4848,#4001,#4002);
#3266=AXIS2_PLACEMENT_3D('',#4851,#4004,#4005);
#3267=AXIS2_PLACEMENT_3D('',#4852,#4006,#4007);
#3268=AXIS2_PLACEMENT_3D('',#4855,#4009,#4010);
#3269=AXIS2_PLACEMENT_3D('',#4856,#4011,#4012);
#3270=AXIS2_PLACEMENT_3D('',#4869,#4019,#4020);
#3271=AXIS2_PLACEMENT_3D('',#4870,#4021,#4022);
#3272=AXIS2_PLACEMENT_3D('',#4871,#4023,#4024);
#3273=AXIS2_PLACEMENT_3D('',#4878,#4029,#4030);
#3274=AXIS2_PLACEMENT_3D('',#4883,#4034,#4035);
#3275=AXIS2_PLACEMENT_3D('',#4888,#4039,#4040);
#3276=AXIS2_PLACEMENT_3D('',#4893,#4044,#4045);
#3277=AXIS2_PLACEMENT_3D('',#4898,#4049,#4050);
#3278=AXIS2_PLACEMENT_3D('',#4901,#4053,#4054);
#3279=AXIS2_PLACEMENT_3D('',#4902,#4055,#4056);
#3280=AXIS2_PLACEMENT_3D('',#4903,#4057,#4058);
#3281=AXIS2_PLACEMENT_3D('',#4904,#4059,#4060);
#3282=AXIS2_PLACEMENT_3D('',#4905,#4061,#4062);
#3283=AXIS2_PLACEMENT_3D('',#4906,#4063,#4064);
#3961=DIRECTION('axis',(0.,0.,1.));
#3962=DIRECTION('refdir',(1.,0.,0.));
#3963=DIRECTION('center_axis',(-1.,0.,0.));
#3964=DIRECTION('ref_axis',(0.,0.,1.));
#3965=DIRECTION('',(-0.500000000000005,-1.0605752387249E-16,-0.866025403784436));
#3966=DIRECTION('center_axis',(-1.,0.,0.));
#3967=DIRECTION('ref_axis',(0.,0.,1.));
#3968=DIRECTION('center_axis',(-1.,0.,0.));
#3969=DIRECTION('ref_axis',(0.,0.,1.));
#3970=DIRECTION('center_axis',(-1.,0.,0.));
#3971=DIRECTION('ref_axis',(0.,0.,1.));
#3972=DIRECTION('center_axis',(-1.,0.,0.));
#3973=DIRECTION('ref_axis',(0.,0.,1.));
#3974=DIRECTION('center_axis',(-1.,0.,0.));
#3975=DIRECTION('ref_axis',(0.,0.,1.));
#3976=DIRECTION('center_axis',(-1.,0.,0.));
#3977=DIRECTION('ref_axis',(0.,0.,1.));
#3978=DIRECTION('center_axis',(-1.,0.,0.));
#3979=DIRECTION('ref_axis',(0.,0.,1.));
#3980=DIRECTION('center_axis',(-1.,0.,0.));
#3981=DIRECTION('ref_axis',(0.,0.,1.));
#3982=DIRECTION('center_axis',(0.,-1.,1.22464679914735E-16));
#3983=DIRECTION('ref_axis',(0.,-1.22464679914735E-16,-1.));
#3984=DIRECTION('center_axis',(1.,0.,0.));
#3985=DIRECTION('ref_axis',(0.,0.,1.));
#3986=DIRECTION('center_axis',(1.,0.,0.));
#3987=DIRECTION('ref_axis',(0.,0.,-1.));
#3988=DIRECTION('center_axis',(1.,0.,0.));
#3989=DIRECTION('ref_axis',(0.,0.,-1.));
#3990=DIRECTION('center_axis',(1.,0.,0.));
#3991=DIRECTION('ref_axis',(0.,0.,-1.));
#3992=DIRECTION('center_axis',(0.,1.,1.22464679914735E-16));
#3993=DIRECTION('ref_axis',(0.,-1.22464679914735E-16,1.));
#3994=DIRECTION('center_axis',(-1.,0.,0.));
#3995=DIRECTION('ref_axis',(0.,0.,-1.));
#3996=DIRECTION('center_axis',(-1.,0.,0.));
#3997=DIRECTION('ref_axis',(0.,0.,1.));
#3998=DIRECTION('',(1.,0.,0.));
#3999=DIRECTION('center_axis',(-1.,0.,0.));
#4000=DIRECTION('ref_axis',(0.,0.,1.));
#4001=DIRECTION('center_axis',(-1.,0.,0.));
#4002=DIRECTION('ref_axis',(0.,0.,1.));
#4003=DIRECTION('',(1.,0.,0.));
#4004=DIRECTION('center_axis',(-1.,0.,0.));
#4005=DIRECTION('ref_axis',(0.,0.,1.));
#4006=DIRECTION('center_axis',(-1.,0.,0.));
#4007=DIRECTION('ref_axis',(0.,0.,1.));
#4008=DIRECTION('',(0.707106781186531,8.65956056235514E-17,0.707106781186564));
#4009=DIRECTION('center_axis',(-1.,0.,0.));
#4010=DIRECTION('ref_axis',(0.,0.,1.));
#4011=DIRECTION('center_axis',(-1.,0.,0.));
#4012=DIRECTION('ref_axis',(0.,0.,1.));
#4013=DIRECTION('',(0.,-0.499999999999999,0.866025403784439));
#4014=DIRECTION('',(0.,1.,-1.47141488612846E-15));
#4015=DIRECTION('',(0.,-0.500000000000001,-0.866025403784438));
#4016=DIRECTION('',(0.,0.499999999999999,-0.866025403784439));
#4017=DIRECTION('',(0.,-1.,1.2874880253624E-15));
#4018=DIRECTION('',(0.,-0.500000000000001,-0.866025403784438));
#4019=DIRECTION('center_axis',(1.,0.,0.));
#4020=DIRECTION('ref_axis',(0.,0.,-1.));
#4021=DIRECTION('center_axis',(1.,0.,0.));
#4022=DIRECTION('ref_axis',(0.,0.,-1.));
#4023=DIRECTION('center_axis',(0.,-0.866025403784439,-0.499999999999999));
#4024=DIRECTION('ref_axis',(0.,0.499999999999999,-0.866025403784439));
#4025=DIRECTION('',(-1.,0.,0.));
#4026=DIRECTION('',(0.,-0.499999999999999,0.866025403784439));
#4027=DIRECTION('',(0.,-0.499999999999999,0.866025403784439));
#4028=DIRECTION('',(-1.,0.,0.));
#4029=DIRECTION('center_axis',(0.,1.47141488612846E-15,1.));
#4030=DIRECTION('ref_axis',(0.,-1.,1.47141488612846E-15));
#4031=DIRECTION('',(0.,1.,-1.47141488612846E-15));
#4032=DIRECTION('',(0.,1.,-1.47141488612846E-15));
#4033=DIRECTION('',(-1.,0.,0.));
#4034=DIRECTION('center_axis',(0.,0.866025403784438,-0.500000000000001));
#4035=DIRECTION('ref_axis',(0.,0.500000000000001,0.866025403784438));
#4036=DIRECTION('',(0.,-0.500000000000001,-0.866025403784438));
#4037=DIRECTION('',(0.,-0.500000000000001,-0.866025403784438));
#4038=DIRECTION('',(-1.,0.,0.));
#4039=DIRECTION('center_axis',(0.,0.866025403784439,0.499999999999999));
#4040=DIRECTION('ref_axis',(0.,-0.499999999999999,0.866025403784439));
#4041=DIRECTION('',(0.,0.499999999999999,-0.866025403784439));
#4042=DIRECTION('',(0.,0.499999999999999,-0.866025403784439));
#4043=DIRECTION('',(-1.,0.,0.));
#4044=DIRECTION('center_axis',(0.,-1.2874880253624E-15,-1.));
#4045=DIRECTION('ref_axis',(0.,1.,-1.2874880253624E-15));
#4046=DIRECTION('',(0.,-1.,1.2874880253624E-15));
#4047=DIRECTION('',(0.,-1.,1.2874880253624E-15));
#4048=DIRECTION('',(-1.,0.,0.));
#4049=DIRECTION('center_axis',(0.,0.866025403784438,-0.500000000000001));
#4050=DIRECTION('ref_axis',(0.,0.500000000000001,0.866025403784438));
#4051=DIRECTION('',(0.,-0.500000000000001,-0.866025403784438));
#4052=DIRECTION('',(0.,-0.500000000000001,-0.866025403784438));
#4053=DIRECTION('center_axis',(1.,0.,0.));
#4054=DIRECTION('ref_axis',(0.,0.,-1.));
#4055=DIRECTION('center_axis',(1.,0.,0.));
#4056=DIRECTION('ref_axis',(0.,0.,-1.));
#4057=DIRECTION('center_axis',(1.,0.,0.));
#4058=DIRECTION('ref_axis',(0.,0.,-1.));
#4059=DIRECTION('center_axis',(1.,0.,0.));
#4060=DIRECTION('ref_axis',(0.,0.,-1.));
#4061=DIRECTION('center_axis',(1.,0.,0.));
#4062=DIRECTION('ref_axis',(0.,0.,-1.));
#4063=DIRECTION('center_axis',(1.,0.,0.));
#4064=DIRECTION('ref_axis',(0.,0.,-1.));
#4814=CARTESIAN_POINT('',(0.,0.,0.));
#4815=CARTESIAN_POINT('Origin',(2.5,0.,0.));
#4816=CARTESIAN_POINT('',(3.67894924968523,0.,0.));
#4817=CARTESIAN_POINT('',(2.5,-2.62905054779003E-15,-2.042));
#4818=CARTESIAN_POINT('',(2.5,-2.50072876385889E-16,-2.042));
#4819=CARTESIAN_POINT('',(2.5,-1.76842387452782,-1.021));
#4820=CARTESIAN_POINT('Origin',(2.5,0.,0.));
#4821=CARTESIAN_POINT('',(2.5,-1.76842387452782,1.021));
#4822=CARTESIAN_POINT('Origin',(2.5,0.,0.));
#4823=CARTESIAN_POINT('',(2.5,3.00462919747432E-15,2.042));
#4824=CARTESIAN_POINT('Origin',(2.5,0.,0.));
#4825=CARTESIAN_POINT('',(2.5,1.76842387452782,1.021));
#4826=CARTESIAN_POINT('Origin',(2.5,0.,0.));
#4827=CARTESIAN_POINT('',(2.5,1.76842387452782,-1.021));
#4828=CARTESIAN_POINT('Origin',(2.5,0.,0.));
#4829=CARTESIAN_POINT('Origin',(2.5,0.,0.));
#4830=CARTESIAN_POINT('Origin',(0.25,0.,0.));
#4831=CARTESIAN_POINT('',(0.,-4.89858719658941E-16,-4.));
#4832=CARTESIAN_POINT('Origin',(0.,0.,0.));
#4833=CARTESIAN_POINT('',(0.25,-5.20474889637625E-16,-4.25));
#4834=CARTESIAN_POINT('Origin',(0.25,-4.89858719658941E-16,-4.));
#4835=CARTESIAN_POINT('Origin',(0.25,0.,0.));
#4836=CARTESIAN_POINT('Origin',(5.2,0.,0.));
#4837=CARTESIAN_POINT('',(5.2,3.06161699786838E-16,-2.5));
#4838=CARTESIAN_POINT('',(5.2,-3.06161699786838E-16,2.5));
#4839=CARTESIAN_POINT('Origin',(5.2,0.,0.));
#4840=CARTESIAN_POINT('Origin',(5.2,0.,0.));
#4841=CARTESIAN_POINT('',(5.,-3.30654635769785E-16,2.7));
#4842=CARTESIAN_POINT('Origin',(5.2,-3.30654635769785E-16,2.7));
#4843=CARTESIAN_POINT('Origin',(5.,0.,0.));
#4844=CARTESIAN_POINT('Origin',(-31.75,0.,0.));
#4845=CARTESIAN_POINT('',(5.,-5.20474889637625E-16,-4.25));
#4846=CARTESIAN_POINT('',(-31.75,-5.20474889637625E-16,-4.25));
#4847=CARTESIAN_POINT('Origin',(5.,0.,0.));
#4848=CARTESIAN_POINT('Origin',(-31.75,0.,0.));
#4849=CARTESIAN_POINT('',(24.555,-3.06161699786838E-16,-2.5));
#4850=CARTESIAN_POINT('',(-31.75,-3.06161699786838E-16,-2.5));
#4851=CARTESIAN_POINT('Origin',(24.555,0.,0.));
#4852=CARTESIAN_POINT('Origin',(25.,0.,0.));
#4853=CARTESIAN_POINT('',(25.,-2.51664917224781E-16,-2.055));
#4854=CARTESIAN_POINT('',(25.,-2.51664917224781E-16,-2.055));
#4855=CARTESIAN_POINT('Origin',(25.,0.,0.));
#4856=CARTESIAN_POINT('Origin',(0.,0.,0.));
#4857=CARTESIAN_POINT('',(0.,2.35789849937043,-1.95156391047391E-15));
#4858=CARTESIAN_POINT('',(0.,1.17894924968522,2.042));
#4859=CARTESIAN_POINT('',(0.,2.35789849937043,-1.95156391047391E-15));
#4860=CARTESIAN_POINT('',(0.,-1.17894924968521,2.042));
#4861=CARTESIAN_POINT('',(0.,-1.17894924968521,2.042));
#4862=CARTESIAN_POINT('',(0.,-2.35789849937043,3.25260651745651E-15));
#4863=CARTESIAN_POINT('',(0.,-1.17894924968521,2.042));
#4864=CARTESIAN_POINT('',(0.,-1.17894924968522,-2.042));
#4865=CARTESIAN_POINT('',(0.,-2.35789849937043,3.25260651745651E-15));
#4866=CARTESIAN_POINT('',(0.,1.17894924968521,-2.042));
#4867=CARTESIAN_POINT('',(0.,1.17894924968521,-2.042));
#4868=CARTESIAN_POINT('',(0.,2.35789849937043,-1.95156391047391E-15));
#4869=CARTESIAN_POINT('Origin',(25.,2.055,0.));
#4870=CARTESIAN_POINT('Origin',(5.,4.25,0.));
#4871=CARTESIAN_POINT('Origin',(2.5,2.35789849937043,-1.95156391047391E-15));
#4872=CARTESIAN_POINT('',(2.5,2.35789849937043,-1.95156391047391E-15));
#4873=CARTESIAN_POINT('',(2.5,2.35789849937043,-1.95156391047391E-15));
#4874=CARTESIAN_POINT('',(2.5,2.35789849937043,-1.95156391047391E-15));
#4875=CARTESIAN_POINT('',(2.5,1.17894924968522,2.042));
#4876=CARTESIAN_POINT('',(2.5,2.35789849937043,-1.95156391047391E-15));
#4877=CARTESIAN_POINT('',(2.5,1.17894924968522,2.042));
#4878=CARTESIAN_POINT('Origin',(2.5,-1.17894924968521,2.042));
#4879=CARTESIAN_POINT('',(2.5,-1.17894924968521,2.042));
#4880=CARTESIAN_POINT('',(2.5,-1.17894924968521,2.042));
#4881=CARTESIAN_POINT('',(2.5,-1.17894924968521,2.042));
#4882=CARTESIAN_POINT('',(2.5,-1.17894924968521,2.042));
#4883=CARTESIAN_POINT('Origin',(2.5,-1.17894924968521,2.042));
#4884=CARTESIAN_POINT('',(2.5,-1.17894924968521,2.042));
#4885=CARTESIAN_POINT('',(2.5,-2.35789849937043,3.25260651745651E-15));
#4886=CARTESIAN_POINT('',(2.5,-1.17894924968521,2.042));
#4887=CARTESIAN_POINT('',(2.5,-2.35789849937043,3.25260651745651E-15));
#4888=CARTESIAN_POINT('Origin',(2.5,-2.35789849937043,3.25260651745651E-15));
#4889=CARTESIAN_POINT('',(2.5,-2.35789849937043,3.25260651745651E-15));
#4890=CARTESIAN_POINT('',(2.5,-1.17894924968522,-2.042));
#4891=CARTESIAN_POINT('',(2.5,-2.35789849937043,3.25260651745651E-15));
#4892=CARTESIAN_POINT('',(2.5,-1.17894924968522,-2.042));
#4893=CARTESIAN_POINT('Origin',(2.5,1.17894924968521,-2.042));
#4894=CARTESIAN_POINT('',(2.5,1.17894924968521,-2.042));
#4895=CARTESIAN_POINT('',(2.5,1.17894924968521,-2.042));
#4896=CARTESIAN_POINT('',(2.5,1.17894924968521,-2.042));
#4897=CARTESIAN_POINT('',(2.5,1.17894924968521,-2.042));
#4898=CARTESIAN_POINT('Origin',(2.5,2.35789849937043,-1.95156391047391E-15));
#4899=CARTESIAN_POINT('',(2.5,2.35789849937043,-1.95156391047391E-15));
#4900=CARTESIAN_POINT('',(2.5,2.35789849937043,-1.95156391047391E-15));
#4901=CARTESIAN_POINT('Origin',(2.5,2.35789849937043,-1.95156391047391E-15));
#4902=CARTESIAN_POINT('Origin',(2.5,2.35789849937043,-1.95156391047391E-15));
#4903=CARTESIAN_POINT('Origin',(2.5,2.35789849937043,-1.95156391047391E-15));
#4904=CARTESIAN_POINT('Origin',(2.5,2.35789849937043,-1.95156391047391E-15));
#4905=CARTESIAN_POINT('Origin',(2.5,2.35789849937043,-1.95156391047391E-15));
#4906=CARTESIAN_POINT('Origin',(2.5,2.35789849937043,-1.95156391047391E-15));
#5678=UNCERTAINTY_MEASURE_WITH_UNIT(LENGTH_MEASURE(0.01),#5690,
'DISTANCE_ACCURACY_VALUE',
'Maximum model space distance between geometric entities at asserted c
onnectivities');
#5680=UNCERTAINTY_MEASURE_WITH_UNIT(LENGTH_MEASURE(0.01),#5690,
'DISTANCE_ACCURACY_VALUE',
'Maximum model space distance between geometric entities at asserted c
onnectivities');
#5687=(
GEOMETRIC_REPRESENTATION_CONTEXT(3)
GLOBAL_UNCERTAINTY_ASSIGNED_CONTEXT((#5678))
GLOBAL_UNIT_ASSIGNED_CONTEXT((#5690,#5692,#5693))
REPRESENTATION_CONTEXT('','3D')
);
#5689=(
GEOMETRIC_REPRESENTATION_CONTEXT(3)
GLOBAL_UNCERTAINTY_ASSIGNED_CONTEXT((#5680))
GLOBAL_UNIT_ASSIGNED_CONTEXT((#5690,#5692,#5693))
REPRESENTATION_CONTEXT('','3D')
);
#5690=(
LENGTH_UNIT()
NAMED_UNIT(*)
SI_UNIT(.MILLI.,.METRE.)
);
#5692=(
NAMED_UNIT(*)
PLANE_ANGLE_UNIT()
SI_UNIT($,.RADIAN.)
);
#5693=(
NAMED_UNIT(*)
SI_UNIT($,.STERADIAN.)
SOLID_ANGLE_UNIT()
);
#5700=SHAPE_DEFINITION_REPRESENTATION(#5708,#5763);
#5708=PRODUCT_DEFINITION_SHAPE('',$,#5772);
#5763=SHAPE_REPRESENTATION('',(#3246),#5687);
#5765=PRODUCT_DEFINITION_CONTEXT('part definition',#5791,'design');
#5772=PRODUCT_DEFINITION(
'socket head cap screw_iso_ISO 4762 M5 x 20 - 20N',
'socket head cap screw_iso_ISO 4762 M5 x 20 - 20N',#5780,#5765);
#5780=PRODUCT_DEFINITION_FORMATION('',$,#5799);
#5791=APPLICATION_CONTEXT(
'Core Data for Automotive Mechanical Design Process');
#5792=PRODUCT_CONTEXT('part definition',#5791,'mechanical');
#5799=PRODUCT('socket head cap screw_iso_ISO 4762 M5 x 20 - 20N',
'socket head cap screw_iso_ISO 4762 M5 x 20 - 20N',$,(#5792));
#5806=PRESENTATION_STYLE_ASSIGNMENT((#5812));
#5812=SURFACE_STYLE_USAGE(.BOTH.,#5818);
#5818=SURFACE_SIDE_STYLE('',(#5824));
#5824=SURFACE_STYLE_FILL_AREA(#5830);
#5830=FILL_AREA_STYLE('Opaque(31,36,43)',(#5836));
#5836=FILL_AREA_STYLE_COLOUR('Opaque(31,36,43)',#5842);
#5842=COLOUR_RGB('Opaque(31,36,43)',0.12156862745098,0.141176470588235,
0.168627450980392);
ENDSEC;
END-ISO-10303-21;
